ISO-10303-21;
HEADER;
FILE_DESCRIPTION (('STEP AP214'),
    '1' );
FILE_NAME ('hex nut style 1_am_B18.2.4.1M - Hex nut, Style 1,  M10 x 1.5, with 16mm WAF --D-N__PD3008.step',
    '2026-10-24T15:53:57',
    ( '' ),
    ( '' ),
    'SwSTEP 2.0',
    'SolidWorks 2025',
    '' );
FILE_SCHEMA (( 'AUTOMOTIVE_DESIGN' ));
ENDSEC;

DATA;
#5=VECTOR ( 'NONE', #7209, 1000.000000000000000 ) ;
#11=CARTESIAN_POINT ( 'NONE',  ( 8.000000000000229150, 4.618802153516954334, -8.400000000000018119 ) ) ;
#16=CARTESIAN_POINT ( 'NONE',  ( 3.319543390096325375, -7.321065037175607415, -8.383111142572088781 ) ) ;
#19=PLANE ( 'NONE',  #5290 ) ;
#23=AXIS2_PLACEMENT_3D ( 'NONE', #7764, #3194, #2455 ) ;
#34=CARTESIAN_POINT ( 'NONE',  ( -3.999999999999892530, 6.928203230275431501, -8.400000000000018119 ) ) ;
#40=MANIFOLD_SOLID_BREP ( 'EndChamfer', #8067 ) ;
#47=EDGE_CURVE ( 'NONE', #2278, #2801, #888, .T. ) ;
#54=B_SPLINE_CURVE_WITH_KNOTS ( 'NONE', 3,
 ( #4820, #7477, #2036, #5217, #8413, #5353 ),
 .UNSPECIFIED., .F., .F.,
 ( 4, 2, 4 ),
 ( 0.008240550023493465118, 0.01057684187039403985, 0.01291313371729461458 ),
 .UNSPECIFIED. ) ;
#61=CARTESIAN_POINT ( 'NONE',  ( 5.690023276062458280, 5.952467836904209442, -0.1306530452038583978 ) ) ;
#71=EDGE_LOOP ( 'NONE', ( #5393, #5239, #6082 ) ) ;
#111=CARTESIAN_POINT ( 'NONE',  ( 2.309976723937863241, -7.903938623647072781, -8.269346954796054305 ) ) ;
#172=DIRECTION ( 'NONE',  ( -0.000000000000000000, -0.000000000000000000, 1.000000000000000000 ) ) ;
#180=AXIS2_PLACEMENT_3D ( 'NONE', #8116, #8071, #4145 ) ;
#187=ORIENTED_EDGE ( 'NONE', *, *, #8140, .F. ) ;
#188=DIRECTION ( 'NONE',  ( -0.8660254037844362651, -0.5000000000000039968, 0.000000000000000000 ) ) ;
#191=ORIENTED_EDGE ( 'NONE', *, *, #5664, .F. ) ;
#200=CARTESIAN_POINT ( 'NONE',  ( 6.686525924292749501, -5.377136764700527927, -8.083279549040062406 ) ) ;
#215=CARTESIAN_POINT ( 'NONE',  ( -7.999999999999785061, 4.618802153516954334, -7.685468820183672278 ) ) ;
#223=CARTESIAN_POINT ( 'NONE',  ( 0.000000000000000000, 0.000000000000000000, -8.401000000000047763 ) ) ;
#229=ORIENTED_EDGE ( 'NONE', *, *, #2672, .F. ) ;
#293=ORIENTED_EDGE ( 'NONE', *, *, #7605, .F. ) ;
#300=ORIENTED_EDGE ( 'NONE', *, *, #47, .F. ) ;
#327=B_SPLINE_CURVE_WITH_KNOTS ( 'NONE', 3,
 ( #6752, #6150, #2862, #1472, #6922, #4786, #4128, #948 ),
 .UNSPECIFIED., .F., .F.,
 ( 4, 2, 2, 4 ),
 ( 0.004673709593152389034, 0.005837709341827845497, 0.007001709090503301092, 0.009329708587854212282 ),
 .UNSPECIFIED. ) ;
#348=DIRECTION ( 'NONE',  ( 0.8660254037844369313, 0.5000000000000028866, 0.000000000000000000 ) ) ;
#388=CARTESIAN_POINT ( 'NONE',  ( -4.000000000000114575, -6.928203230275542523, -8.400000000000018119 ) ) ;
#392=FACE_OUTER_BOUND ( 'NONE', #493, .T. ) ;
#393=ORIENTED_EDGE ( 'NONE', *, *, #1927, .F. ) ;
#402=EDGE_CURVE ( 'NONE', #7042, #3286, #2933, .T. ) ;
#408=CARTESIAN_POINT ( 'NONE',  ( -6.686525924292650025, 5.377136764700151339, -8.083279549040247147 ) ) ;
#413=CARTESIAN_POINT ( 'NONE',  ( -4.000000000000114575, -6.928203230275542523, -8.400000000000018119 ) ) ;
#414=CONICAL_SURFACE ( 'NONE', #3326, 8.000000000000007105, 1.047197551196597631 ) ;
#424=EDGE_CURVE ( 'NONE', #2278, #1504, #1016, .T. ) ;
#428=CARTESIAN_POINT ( 'NONE',  ( 4.000000000000003553, 6.928203230275597591, 0.000000000000000000 ) ) ;
#433=CARTESIAN_POINT ( 'NONE',  ( -7.347286611336967255, -4.995646404165273502, -7.903039949738268177 ) ) ;
#442=ORIENTED_EDGE ( 'NONE', *, *, #3742, .F. ) ;
#444=DIRECTION ( 'NONE',  ( 1.000000000000000000, 8.881784197001244435E-16, 0.000000000000000000 ) ) ;
#446=UNCERTAINTY_MEASURE_WITH_UNIT (LENGTH_MEASURE( 1.000000000000000082E-05 ), #3151, 'distance_accuracy_value', 'NONE');
#453=DIRECTION ( 'NONE',  ( -1.000000000000000000, 6.572520305780926719E-14, 0.000000000000000000 ) ) ;
#455=EDGE_CURVE ( 'NONE', #2278, #7258, #7612, .T. ) ;
#464=CARTESIAN_POINT ( 'NONE',  ( -2.644994884458949702, 7.710515798486381023, -0.08224679563969222729 ) ) ;
#493=EDGE_LOOP ( 'NONE', ( #6950, #6237, #3890, #3563, #7554, #2080 ) ) ;
#510=FACE_OUTER_BOUND ( 'NONE', #7059, .T. ) ;
#516=DIRECTION ( 'NONE',  ( 0.000000000000000000, 0.000000000000000000, 1.000000000000000000 ) ) ;
#532=LINE ( 'NONE', #5149, #5435 ) ;
#536=ADVANCED_FACE ( 'NONE', ( #7444 ), #6518, .T. ) ;
#544=DIRECTION ( 'NONE',  ( 1.000000000000000000, 8.881784197001244435E-16, 0.000000000000000000 ) ) ;
#559=EDGE_CURVE ( 'NONE', #3935, #2131, #2494, .T. ) ;
#570=CARTESIAN_POINT ( 'NONE',  ( 0.000000000000000000, 0.000000000000000000, -8.400000000000018119 ) ) ;
#576=EDGE_CURVE ( 'NONE', #3286, #2515, #327, .T. ) ;
#585=AXIS2_PLACEMENT_3D ( 'NONE', #5412, #4182, #1358 ) ;
#589=CIRCLE ( 'NONE', #7410, 5.500000000000023981 ) ;
#604=CARTESIAN_POINT ( 'NONE',  ( -7.999999999999896083, 3.871967595402076689, -7.901061386767628925 ) ) ;
#606=CARTESIAN_POINT ( 'NONE',  ( 4.000000000000225597, -6.928203230275542523, -8.400000000000018119 ) ) ;
#611=CARTESIAN_POINT ( 'NONE',  ( -5.080504117408895404, -2.106769544347820933, 0.000000000000000000 ) ) ;
#626=( NAMED_UNIT ( * ) SI_UNIT ( $, .STERADIAN. ) SOLID_ANGLE_UNIT ( ) );
#635=CARTESIAN_POINT ( 'NONE',  ( -3.318518101603071369, -7.321656987762848345, 3.872634634846659572E-15 ) ) ;
#650=VERTEX_POINT ( 'NONE', #7651 ) ;
#655=ORIENTED_EDGE ( 'NONE', *, *, #7198, .T. ) ;
#676=CARTESIAN_POINT ( 'NONE',  ( 7.999999999999674039, -4.618802153517231446, -7.685468820183672278 ) ) ;
#687=DIRECTION ( 'NONE',  ( 1.000000000000000000, 8.881784197001244435E-16, 0.000000000000000000 ) ) ;
#690=CARTESIAN_POINT ( 'NONE',  ( -3.999999999999892530, 6.928203230275431501, 0.000000000000000000 ) ) ;
#712=ORIENTED_EDGE ( 'NONE', *, *, #1927, .T. ) ;
#713=CARTESIAN_POINT ( 'NONE',  ( 8.000000000000232703, 3.115336682266936830, -8.080606868608402493 ) ) ;
#742=DIRECTION ( 'NONE',  ( 0.000000000000000000, 0.000000000000000000, -1.000000000000000000 ) ) ;
#763=AXIS2_PLACEMENT_3D ( 'NONE', #5818, #6378, #8446 ) ;
#785=EDGE_LOOP ( 'NONE', ( #1709, #6316, #7907 ) ) ;
#788=FACE_OUTER_BOUND ( 'NONE', #1413, .T. ) ;
#819=( NAMED_UNIT ( * ) PLANE_ANGLE_UNIT ( ) SI_UNIT ( $, .RADIAN. ) );
#825=DIRECTION ( 'NONE',  ( -0.9237280213470678847, -0.3830490080632384942, 0.000000000000000000 ) ) ;
#831=CARTESIAN_POINT ( 'NONE',  ( -7.999999999999890754, -3.098204225878261386, -0.3157906771918332911 ) ) ;
#842=CARTESIAN_POINT ( 'NONE',  ( 0.6527133886632224824, -8.860760056385986516, -0.4969600502619001547 ) ) ;
#850=ORIENTED_EDGE ( 'NONE', *, *, #6226, .F. ) ;
#888=CIRCLE ( 'NONE', #2697, 8.000000000000007105 ) ;
#902=VERTEX_POINT ( 'NONE', #2666 ) ;
#924=B_SPLINE_CURVE_WITH_KNOTS ( 'NONE', 3,
 ( #7808, #3236, #3155, #464, #3111, #8429, #4459, #7121 ),
 .UNSPECIFIED., .F., .F.,
 ( 4, 2, 2, 4 ),
 ( 0.004673709593152105407, 0.005837709341827623452, 0.007001709090503142364, 0.009329708587854177587 ),
 .UNSPECIFIED. ) ;
#926=CARTESIAN_POINT ( 'NONE',  ( 0.6543471694414046969, 8.859816792613671055, -7.903584543331200862 ) ) ;
#948=CARTESIAN_POINT ( 'NONE',  ( -8.000000000000007105, -4.618802153517065356, -0.7145311798163467287 ) ) ;
#967=FACE_OUTER_BOUND ( 'NONE', #6917, .T. ) ;
#969=CARTESIAN_POINT ( 'NONE',  ( 3.318518101603053161, 7.321656987762952262, -8.399999999999966604 ) ) ;
#986=AXIS2_PLACEMENT_3D ( 'NONE', #223, #2880, #5550 ) ;
#1012=B_SPLINE_CURVE_WITH_KNOTS ( 'NONE', 3,
 ( #2126, #926, #1610, #4274, #969, #2969 ),
 .UNSPECIFIED., .F., .F.,
 ( 4, 2, 4 ),
 ( 2.380731633597212072E-07, 0.002336973833157672195, 0.004673709593151984844 ),
 .UNSPECIFIED. ) ;
#1016=CIRCLE ( 'NONE', #3515, 8.000000000000007105 ) ;
#1020=ORIENTED_EDGE ( 'NONE', *, *, #2966, .T. ) ;
#1056=DIRECTION ( 'NONE',  ( -0.000000000000000000, -0.000000000000000000, 1.000000000000000000 ) ) ;
#1072=DIRECTION ( 'NONE',  ( 0.000000000000000000, 0.000000000000000000, -1.000000000000000000 ) ) ;
#1075=CONICAL_SURFACE ( 'NONE', #8033, 8.000000000000007105, 1.047197551196597631 ) ;
#1080=ADVANCED_FACE ( 'NONE', ( #3746 ), #5169, .F. ) ;
#1103=ORIENTED_EDGE ( 'NONE', *, *, #2966, .F. ) ;
#1128=ORIENTED_EDGE ( 'NONE', *, *, #2618, .F. ) ;
#1138=DIRECTION ( 'NONE',  ( 0.000000000000000000, 0.000000000000000000, -1.000000000000000000 ) ) ;
#1156=CARTESIAN_POINT ( 'NONE',  ( -0.6543471694412575923, -8.859816792613658620, -0.4964154566688018799 ) ) ;
#1160=EDGE_LOOP ( 'NONE', ( #4751, #8064 ) ) ;
#1163=AXIS2_PLACEMENT_3D ( 'NONE', #8403, #4472, #516 ) ;
#1177=LINE ( 'NONE', #1828, #3923 ) ;
#1184=B_SPLINE_CURVE_WITH_KNOTS ( 'NONE', 3,
 ( #606, #1997, #16, #3959, #111, #5450, #4660, #5398 ),
 .UNSPECIFIED., .F., .F.,
 ( 4, 2, 2, 4 ),
 ( 0.004673709593152015201, 0.005837709341827572278, 0.007001709090503129354, 0.009329708587854243507 ),
 .UNSPECIFIED. ) ;
#1188=ORIENTED_EDGE ( 'NONE', *, *, #7824, .F. ) ;
#1217=CARTESIAN_POINT ( 'NONE',  ( 8.000000000000117240, -1.110223024625156540E-13, 0.000000000000000000 ) ) ;
#1224=CARTESIAN_POINT ( 'NONE',  ( 8.000000000000232703, 0.7809653281575155148, -8.399999999999890221 ) ) ;
#1242=PLANE ( 'NONE',  #6638 ) ;
#1246=CARTESIAN_POINT ( 'NONE',  ( -8.000000000000117240, -1.110223024625156540E-13, -8.400000000000018119 ) ) ;
#1252=ORIENTED_EDGE ( 'NONE', *, *, #6887, .F. ) ;
#1266=EDGE_CURVE ( 'NONE', #8505, #6546, #8013, .T. ) ;
#1268=EDGE_CURVE ( 'NONE', #2856, #3046, #7904, .T. ) ;
#1274=ORIENTED_EDGE ( 'NONE', *, *, #6405, .T. ) ;
#1292=CARTESIAN_POINT ( 'NONE',  ( 8.000000000000229150, 4.618802153516954334, -8.400000000000018119 ) ) ;
#1296=CARTESIAN_POINT ( 'NONE',  ( 8.000000000000234479, 3.115336682266935497, -0.3193931313916126280 ) ) ;
#1350=CARTESIAN_POINT ( 'NONE',  ( -3.318518101603071369, -7.321656987762848345, -8.400000000000021672 ) ) ;
#1358=DIRECTION ( 'NONE',  ( -1.000000000000000000, -8.881784197001244435E-16, 0.000000000000000000 ) ) ;
#1363=CARTESIAN_POINT ( 'NONE',  ( 0.000000000000000000, -9.237604307034018802, -0.7145311798163467287 ) ) ;
#1377=CARTESIAN_POINT ( 'NONE',  ( 7.347286611337072948, 4.995646404165303700, -0.4969600502618077842 ) ) ;
#1382=DIRECTION ( 'NONE',  ( 0.000000000000000000, 0.000000000000000000, 1.000000000000000000 ) ) ;
#1413=EDGE_LOOP ( 'NONE', ( #7381, #1188, #6826 ) ) ;
#1414=CARTESIAN_POINT ( 'NONE',  ( 4.000000000000003553, 6.928203230275597591, 0.000000000000000000 ) ) ;
#1430=CARTESIAN_POINT ( 'NONE',  ( 5.355005115540953931, 6.145890662064713794, -0.08224679563976165786 ) ) ;
#1460=CARTESIAN_POINT ( 'NONE',  ( 2.220446049250313081E-13, 9.237604307034075646, -8.400000000000018119 ) ) ;
#1467=VERTEX_POINT ( 'NONE', #7446 ) ;
#1472=CARTESIAN_POINT ( 'NONE',  ( -5.355005115540942384, -6.145890662064630305, -0.08224679563972098206 ) ) ;
#1504=VERTEX_POINT ( 'NONE', #428 ) ;
#1508=CARTESIAN_POINT ( 'NONE',  ( 3.660532965669080152, -7.124194613927820718, -1.655712242656924192E-13 ) ) ;
#1516=CARTESIAN_POINT ( 'NONE',  ( -7.999999999999888978, -3.867591403079263301, -0.4976753153245478956 ) ) ;
#1519=CIRCLE ( 'NONE', #6958, 8.000000000000007105 ) ;
#1538=FACE_OUTER_BOUND ( 'NONE', #2078, .T. ) ;
#1541=CONICAL_SURFACE ( 'NONE', #3775, 8.000000000000007105, 1.047197551196597631 ) ;
#1548=ORIENTED_EDGE ( 'NONE', *, *, #5643, .F. ) ;
#1571=CONICAL_SURFACE ( 'NONE', #180, 8.000000000000007105, 1.047197551196597631 ) ;
#1586=EDGE_LOOP ( 'NONE', ( #187, #442, #4171, #300, #6467, #2482 ) ) ;
#1610=CARTESIAN_POINT ( 'NONE',  ( 1.313474075707348421, 8.479269695850897293, -8.083279549040144119 ) ) ;
#1662=CARTESIAN_POINT ( 'NONE',  ( 0.000000000000000000, 0.000000000000000000, -8.400000000000018119 ) ) ;
#1695=CARTESIAN_POINT ( 'NONE',  ( 0.000000000000000000, 0.000000000000000000, -8.400000000000018119 ) ) ;
#1703=CIRCLE ( 'NONE', #7427, 8.000000000000007105 ) ;
#1709=ORIENTED_EDGE ( 'NONE', *, *, #4035, .T. ) ;
#1710=CIRCLE ( 'NONE', #585, 8.000000000000007105 ) ;
#1727=ORIENTED_EDGE ( 'NONE', *, *, #2733, .T. ) ;
#1739=CARTESIAN_POINT ( 'NONE',  ( 0.000000000000000000, 0.000000000000000000, -8.401000000000047763 ) ) ;
#1743=B_SPLINE_CURVE_WITH_KNOTS ( 'NONE', 3,
 ( #1846, #7165, #3937, #3891, #3197, #5884, #7206, #6550 ),
 .UNSPECIFIED., .F., .F.,
 ( 4, 2, 2, 4 ),
 ( 0.004673709593151984844, 0.005837709341827513297, 0.007001709090503041751, 0.009329708587854099525 ),
 .UNSPECIFIED. ) ;
#1762=B_SPLINE_CURVE_WITH_KNOTS ( 'NONE', 3,
 ( #8015, #1516, #831, #7967, #5452, #4706 ),
 .UNSPECIFIED., .F., .F.,
 ( 4, 2, 4 ),
 ( 0.008240550023493596957, 0.01057684187039410230, 0.01291313371729460764 ),
 .UNSPECIFIED. ) ;
#1767=CARTESIAN_POINT ( 'NONE',  ( -6.689127551062020949, -5.375634714784609081, -8.082649155111361949 ) ) ;
#1773=CARTESIAN_POINT ( 'NONE',  ( 2.644994884459373363, -7.710515798486559547, -0.08224679563987125075 ) ) ;
#1777=FACE_OUTER_BOUND ( 'NONE', #71, .T. ) ;
#1810=CARTESIAN_POINT ( 'NONE',  ( 0.000000000000000000, -9.237604307034018802, -0.7145311798163467287 ) ) ;
#1814=ORIENTED_EDGE ( 'NONE', *, *, #1268, .F. ) ;
#1820=ORIENTED_EDGE ( 'NONE', *, *, #2733, .F. ) ;
#1821=CARTESIAN_POINT ( 'NONE',  ( 0.000000000000000000, 0.000000000000000000, -8.400000000000018119 ) ) ;
#1828=CARTESIAN_POINT ( 'NONE',  ( 7.999999999999674039, -4.618802153517231446, -8.400000000000018119 ) ) ;
#1840=CIRCLE ( 'NONE', #23, 8.000000000000007105 ) ;
#1846=CARTESIAN_POINT ( 'NONE',  ( 4.000000000000003553, 6.928203230275597591, -8.400000000000018119 ) ) ;
#1854=CARTESIAN_POINT ( 'NONE',  ( -1.310872448937806745, 8.480771745766437775, -8.082649155111361949 ) ) ;
#1859=B_SPLINE_CURVE_WITH_KNOTS ( 'NONE', 3,
 ( #3081, #6795, #6653, #1430, #61, #2774, #1377, #2032 ),
 .UNSPECIFIED., .F., .F.,
 ( 4, 2, 2, 4 ),
 ( 0.004673709593151983109, 0.005837709341827512430, 0.007001709090503040883, 0.009329708587854099525 ),
 .UNSPECIFIED. ) ;
#1874=CONICAL_SURFACE ( 'NONE', #8141, 8.000000000000007105, 1.047197551196597631 ) ;
#1877=CARTESIAN_POINT ( 'NONE',  ( 8.000000000000234479, -0.7805016046292200249, -1.407040310002008213E-13 ) ) ;
#1884=ORIENTED_EDGE ( 'NONE', *, *, #5073, .T. ) ;
#1897=CARTESIAN_POINT ( 'NONE',  ( -7.999999999999785061, -4.618802153517121312, -8.400000000000018119 ) ) ;
#1898=CARTESIAN_POINT ( 'NONE',  ( -2.309976723937442245, 7.903938623646887152, -8.269346954796224836 ) ) ;
#1927=EDGE_CURVE ( 'NONE', #5903, #2515, #2855, .T. ) ;
#1941=EDGE_LOOP ( 'NONE', ( #8445, #8072, #6080 ) ) ;
#1957=ORIENTED_EDGE ( 'NONE', *, *, #3170, .T. ) ;
#1960=DIRECTION ( 'NONE',  ( -1.000000000000000000, -8.881784197001244435E-16, 0.000000000000000000 ) ) ;
#1973=ORIENTED_EDGE ( 'NONE', *, *, #7824, .T. ) ;
#1982=CARTESIAN_POINT ( 'NONE',  ( 0.000000000000000000, 0.000000000000000000, -8.400000000000018119 ) ) ;
#1986=DIRECTION ( 'NONE',  ( 0.000000000000000000, 0.000000000000000000, -1.000000000000000000 ) ) ;
#1990=DIRECTION ( 'NONE',  ( -0.8660254037844365982, 0.5000000000000035527, -0.000000000000000000 ) ) ;
#1997=CARTESIAN_POINT ( 'NONE',  ( 3.660532965669079708, -7.124194613927820718, -8.399999999999852918 ) ) ;
#2000=FACE_BOUND ( 'NONE', #8112, .T. ) ;
#2003=CARTESIAN_POINT ( 'NONE',  ( -0.6543471694412575923, -8.859816792613658620, -7.903584543331218626 ) ) ;
#2005=DIRECTION ( 'NONE',  ( 0.000000000000000000, 0.000000000000000000, 1.000000000000000000 ) ) ;
#2011=VERTEX_POINT ( 'NONE', #413 ) ;
#2031=ORIENTED_EDGE ( 'NONE', *, *, #3184, .F. ) ;
#2032=CARTESIAN_POINT ( 'NONE',  ( 8.000000000000117240, 4.618802153517009401, -0.7145311798163467287 ) ) ;
#2033=FACE_OUTER_BOUND ( 'NONE', #6919, .T. ) ;
#2036=CARTESIAN_POINT ( 'NONE',  ( 8.000000000000238032, -3.098204225878338658, -8.084209322807982545 ) ) ;
#2038=EDGE_CURVE ( 'NONE', #2131, #3744, #3892, .T. ) ;
#2063=B_SPLINE_CURVE_WITH_KNOTS ( 'NONE', 3,
 ( #7881, #5504, #4619, #3398, #4002, #7271 ),
 .UNSPECIFIED., .F., .F.,
 ( 4, 2, 4 ),
 ( 0.008240550023493595222, 0.01057684187039410403, 0.01291313371729461111 ),
 .UNSPECIFIED. ) ;
#2064=CARTESIAN_POINT ( 'NONE',  ( 2.220446049250313081E-13, 9.237604307034075646, -0.7145311798163467287 ) ) ;
#2068=CARTESIAN_POINT ( 'NONE',  ( -5.080504117408889186, -2.106769544347818268, -8.400000000000018119 ) ) ;
#2070=PLANE ( 'NONE',  #4205 ) ;
#2075=DIRECTION ( 'NONE',  ( 0.000000000000000000, 0.000000000000000000, 1.000000000000000000 ) ) ;
#2078=EDGE_LOOP ( 'NONE', ( #6598, #229, #4268, #4956, #4753, #4271 ) ) ;
#2079=CARTESIAN_POINT ( 'NONE',  ( -7.999999999999888978, 0.7809653281574794326, 6.859442213454772481E-14 ) ) ;
#2080=ORIENTED_EDGE ( 'NONE', *, *, #559, .F. ) ;
#2106=ORIENTED_EDGE ( 'NONE', *, *, #5643, .T. ) ;
#2123=PLANE ( 'NONE',  #7963 ) ;
#2126=CARTESIAN_POINT ( 'NONE',  ( 2.220446049250313081E-13, 9.237604307034075646, -7.685468820183672278 ) ) ;
#2131=VERTEX_POINT ( 'NONE', #5194 ) ;
#2140=LINE ( 'NONE', #7448, #4017 ) ;
#2147=CARTESIAN_POINT ( 'NONE',  ( -4.000000000000114575, -6.928203230275542523, 0.000000000000000000 ) ) ;
#2188=ORIENTED_EDGE ( 'NONE', *, *, #6939, .T. ) ;
#2208=ADVANCED_FACE ( 'NONE', ( #3543 ), #4063, .F. ) ;
#2225=ORIENTED_EDGE ( 'NONE', *, *, #5179, .F. ) ;
#2270=AXIS2_PLACEMENT_3D ( 'NONE', #6878, #8175, #4906 ) ;
#2278=VERTEX_POINT ( 'NONE', #6380 ) ;
#2293=CARTESIAN_POINT ( 'NONE',  ( 5.354491962338240540, -6.146186931204690396, -8.331901280394420795 ) ) ;
#2316=CARTESIAN_POINT ( 'NONE',  ( -5.354491962338013167, 6.146186931204386639, -8.331901280394641063 ) ) ;
#2338=VERTEX_POINT ( 'NONE', #6941 ) ;
#2341=DIRECTION ( 'NONE',  ( 0.000000000000000000, 0.000000000000000000, 1.000000000000000000 ) ) ;
#2343=B_SPLINE_CURVE_WITH_KNOTS ( 'NONE', 3,
 ( #7443, #1508, #7741, #1773, #3786, #6814, #842, #1363 ),
 .UNSPECIFIED., .F., .F.,
 ( 4, 2, 2, 4 ),
 ( 0.004673709593152015201, 0.005837709341827571410, 0.007001709090503128487, 0.009329708587854243507 ),
 .UNSPECIFIED. ) ;
#2353=SHAPE_DEFINITION_REPRESENTATION ( #7095, #3455 ) ;
#2362=EDGE_LOOP ( 'NONE', ( #5266, #2365, #7513 ) ) ;
#2365=ORIENTED_EDGE ( 'NONE', *, *, #6226, .T. ) ;
#2394=CYLINDRICAL_SURFACE ( 'NONE', #4225, 5.500000000000023981 ) ;
#2415=CIRCLE ( 'NONE', #2819, 8.000000000000007105 ) ;
#2426=CARTESIAN_POINT ( 'NONE',  ( -2.644994884458948814, 7.710515798486379246, -8.317753204360325725 ) ) ;
#2445=CARTESIAN_POINT ( 'NONE',  ( 7.345652830558639046, -4.996589667937789692, -0.4964154566688734338 ) ) ;
#2451=B_SPLINE_CURVE_WITH_KNOTS ( 'NONE', 3,
 ( #2064, #4721, #2583, #6002, #7290, #1414 ),
 .UNSPECIFIED., .F., .F.,
 ( 4, 2, 4 ),
 ( 2.380731633596903170E-07, 0.002336973833157671328, 0.004673709593151983109 ),
 .UNSPECIFIED. ) ;
#2455=DIRECTION ( 'NONE',  ( -1.000000000000000000, -8.881784197001244435E-16, 0.000000000000000000 ) ) ;
#2462=DIRECTION ( 'NONE',  ( -1.000000000000000000, -8.881784197001244435E-16, 0.000000000000000000 ) ) ;
#2482=ORIENTED_EDGE ( 'NONE', *, *, #2561, .F. ) ;
#2486=AXIS2_PLACEMENT_3D ( 'NONE', #6799, #6233, #825 ) ;
#2487=CARTESIAN_POINT ( 'NONE',  ( -7.345652830558607960, 4.996589667937374912, -7.903584543331300338 ) ) ;
#2494=B_SPLINE_CURVE_WITH_KNOTS ( 'NONE', 3,
 ( #6192, #3436, #200, #2293, #5626, #4949 ),
 .UNSPECIFIED., .F., .F.,
 ( 4, 2, 4 ),
 ( 2.380731633751139929E-07, 0.002336973833157695180, 0.004673709593152015201 ),
 .UNSPECIFIED. ) ;
#2515=VERTEX_POINT ( 'NONE', #5514 ) ;
#2530=B_SPLINE_CURVE_WITH_KNOTS ( 'NONE', 3,
 ( #5765, #8397, #3165, #2426, #1898, #1854, #7733, #5077 ),
 .UNSPECIFIED., .F., .F.,
 ( 4, 2, 2, 4 ),
 ( 0.004673709593152105407, 0.005837709341827624319, 0.007001709090503143232, 0.009329708587854177587 ),
 .UNSPECIFIED. ) ;
#2538=AXIS2_PLACEMENT_3D ( 'NONE', #4621, #742, #1960 ) ;
#2543=EDGE_LOOP ( 'NONE', ( #712, #1727, #7595, #7600, #4582, #2031 ) ) ;
#2552=CARTESIAN_POINT ( 'NONE',  ( 0.000000000000000000, 0.000000000000000000, 0.000000000000000000 ) ) ;
#2561=EDGE_CURVE ( 'NONE', #3046, #1504, #1519, .T. ) ;
#2571=CARTESIAN_POINT ( 'NONE',  ( -1.313474075707240729, -8.479269695850863542, -8.083279549040174317 ) ) ;
#2579=AXIS2_PLACEMENT_3D ( 'NONE', #1897, #6474, #7999 ) ;
#2583=CARTESIAN_POINT ( 'NONE',  ( 1.313474075707348421, 8.479269695850897293, -0.3167204509598749440 ) ) ;
#2585=SHAPE_REPRESENTATION_RELATIONSHIP ( 'NONE' , 'NONE' ,  #3455, #4586 ) ;
#2594=CARTESIAN_POINT ( 'NONE',  ( 0.000000000000000000, 0.000000000000000000, 0.000000000000000000 ) ) ;
#2596=ADVANCED_FACE ( 'NONE', ( #6383 ), #3880, .T. ) ;
#2599=B_SPLINE_CURVE_WITH_KNOTS ( 'NONE', 3,
 ( #3677, #2445, #5983, #7717, #7632, #7758 ),
 .UNSPECIFIED., .F., .F.,
 ( 4, 2, 4 ),
 ( 2.380731633751448567E-07, 0.002336973833157695180, 0.004673709593152015201 ),
 .UNSPECIFIED. ) ;
#2601=CARTESIAN_POINT ( 'NONE',  ( 8.000000000000229150, 3.871967595402074913, -0.4989386132325618339 ) ) ;
#2607=EDGE_CURVE ( 'NONE', #2608, #2801, #2599, .T. ) ;
#2608=VERTEX_POINT ( 'NONE', #6342 ) ;
#2618=EDGE_CURVE ( 'NONE', #6546, #3749, #4158, .T. ) ;
#2648=LINE ( 'NONE', #11, #4540 ) ;
#2651=CARTESIAN_POINT ( 'NONE',  ( 4.000000000000003553, 6.928203230275597591, -8.400000000000018119 ) ) ;
#2652=CARTESIAN_POINT ( 'NONE',  ( -7.999999999999888978, 0.7809653281574864270, -8.400000000000089173 ) ) ;
#2666=CARTESIAN_POINT ( 'NONE',  ( 2.220446049250313081E-13, 9.237604307034075646, -7.685468820183672278 ) ) ;
#2672=EDGE_CURVE ( 'NONE', #3749, #8505, #3063, .T. ) ;
#2686=AXIS2_PLACEMENT_3D ( 'NONE', #8023, #172, #5457 ) ;
#2688=CARTESIAN_POINT ( 'NONE',  ( 8.000000000000117240, 4.618802153517009401, -0.7145311798163467287 ) ) ;
#2689=PLANE ( 'NONE',  #2579 ) ;
#2697=AXIS2_PLACEMENT_3D ( 'NONE', #2594, #1986, #4693 ) ;
#2702=DIRECTION ( 'NONE',  ( 0.000000000000000000, 0.000000000000000000, -1.000000000000000000 ) ) ;
#2706=CARTESIAN_POINT ( 'NONE',  ( 0.000000000000000000, -9.237604307034018802, -7.685468820183672278 ) ) ;
#2721=AXIS2_PLACEMENT_3D ( 'NONE', #3006, #1056, #8321 ) ;
#2725=ADVANCED_FACE ( 'NONE', ( #2000, #3349 ), #19, .F. ) ;
#2733=EDGE_CURVE ( 'NONE', #2515, #650, #1762, .T. ) ;
#2765=B_SPLINE_CURVE_WITH_KNOTS ( 'NONE', 3,
 ( #6593, #1224, #6684, #713, #8585, #8032 ),
 .UNSPECIFIED., .F., .F.,
 ( 4, 2, 4 ),
 ( 0.01291313371729461458, 0.01525081363757315941, 0.01758849355785170598 ),
 .UNSPECIFIED. ) ;
#2774=CARTESIAN_POINT ( 'NONE',  ( 6.689127551062092003, 5.375634714784659707, -0.3173508448887064071 ) ) ;
#2778=CARTESIAN_POINT ( 'NONE',  ( -6.686525924292721079, 5.377136764700112259, -0.3167204509597890683 ) ) ;
#2801=VERTEX_POINT ( 'NONE', #3704 ) ;
#2817=CARTESIAN_POINT ( 'NONE',  ( -7.999999999999896083, 4.618802153516899267, -0.7145311798163467287 ) ) ;
#2819=AXIS2_PLACEMENT_3D ( 'NONE', #4626, #7237, #3919 ) ;
#2855=LINE ( 'NONE', #5521, #4020 ) ;
#2856=VERTEX_POINT ( 'NONE', #6885 ) ;
#2862=CARTESIAN_POINT ( 'NONE',  ( -4.680456609904036114, -6.535341423375559344, -0.01688885742777373675 ) ) ;
#2875=ADVANCED_FACE ( 'NONE', ( #392 ), #5726, .T. ) ;
#2880=DIRECTION ( 'NONE',  ( 0.000000000000000000, 0.000000000000000000, 1.000000000000000000 ) ) ;
#2932=DIRECTION ( 'NONE',  ( 0.000000000000000000, 0.000000000000000000, 1.000000000000000000 ) ) ;
#2933=B_SPLINE_CURVE_WITH_KNOTS ( 'NONE', 3,
 ( #1810, #1156, #5158, #7815, #635, #6693 ),
 .UNSPECIFIED., .F., .F.,
 ( 4, 2, 4 ),
 ( 2.380731631918482768E-07, 0.002336973833157790156, 0.004673709593152389034 ),
 .UNSPECIFIED. ) ;
#2966=EDGE_CURVE ( 'NONE', #1504, #7258, #1859, .T. ) ;
#2969=CARTESIAN_POINT ( 'NONE',  ( 4.000000000000003553, 6.928203230275597591, -8.400000000000018119 ) ) ;
#2988=EDGE_CURVE ( 'NONE', #650, #2856, #5832, .T. ) ;
#3006=CARTESIAN_POINT ( 'NONE',  ( 0.000000000000000000, 0.000000000000000000, -8.400000000000018119 ) ) ;
#3008=PRODUCT_DEFINITION ( 'UNKNOWN', '', #3962, #8224 ) ;
#3010=CARTESIAN_POINT ( 'NONE',  ( 7.999999999999674039, -4.618802153517231446, -0.7145311798163467287 ) ) ;
#3025=EDGE_LOOP ( 'NONE', ( #4964, #1957, #4715 ) ) ;
#3033=CARTESIAN_POINT ( 'NONE',  ( 0.000000000000000000, 0.000000000000000000, 0.000000000000000000 ) ) ;
#3039=ORIENTED_EDGE ( 'NONE', *, *, #7605, .T. ) ;
#3046=VERTEX_POINT ( 'NONE', #5570 ) ;
#3056=AXIS2_PLACEMENT_3D ( 'NONE', #7069, #4328, #4971 ) ;
#3063=CIRCLE ( 'NONE', #4449, 8.000000000000007105 ) ;
#3068=ORIENTED_EDGE ( 'NONE', *, *, #3170, .F. ) ;
#3081=CARTESIAN_POINT ( 'NONE',  ( 4.000000000000003553, 6.928203230275597591, 0.000000000000000000 ) ) ;
#3105=VERTEX_POINT ( 'NONE', #2706 ) ;
#3109=VERTEX_POINT ( 'NONE', #611 ) ;
#3111=CARTESIAN_POINT ( 'NONE',  ( -2.309976723937442689, 7.903938623646887152, -0.1306530452037944767 ) ) ;
#3140=DIRECTION ( 'NONE',  ( -0.000000000000000000, -0.000000000000000000, 1.000000000000000000 ) ) ;
#3142=CARTESIAN_POINT ( 'NONE',  ( -7.999999999999785061, 4.618802153516954334, -7.685468820183672278 ) ) ;
#3151=( LENGTH_UNIT ( ) NAMED_UNIT ( * ) SI_UNIT ( .MILLI., .METRE. ) );
#3155=CARTESIAN_POINT ( 'NONE',  ( -3.319543390095889723, 7.321065037175431556, -0.01688885742773474710 ) ) ;
#3163=CARTESIAN_POINT ( 'NONE',  ( -4.680456609904036114, -6.535341423375559344, -8.383111142572246877 ) ) ;
#3165=CARTESIAN_POINT ( 'NONE',  ( -3.319543390095888835, 7.321065037175429779, -8.383111142572282404 ) ) ;
#3168=CIRCLE ( 'NONE', #5399, 8.000000000000007105 ) ;
#3170=EDGE_CURVE ( 'NONE', #3105, #2011, #8405, .T. ) ;
#3184=EDGE_CURVE ( 'NONE', #5903, #8505, #2063, .T. ) ;
#3194=DIRECTION ( 'NONE',  ( -0.000000000000000000, -0.000000000000000000, 1.000000000000000000 ) ) ;
#3197=CARTESIAN_POINT ( 'NONE',  ( 5.690023276062460056, 5.952467836904209442, -8.269346954796159110 ) ) ;
#3218=ORIENTED_EDGE ( 'NONE', *, *, #4035, .F. ) ;
#3235=VERTEX_POINT ( 'NONE', #5404 ) ;
#3236=CARTESIAN_POINT ( 'NONE',  ( -3.660532965668689354, 7.124194613927617326, 4.229404912230172453E-14 ) ) ;
#3264=ADVANCED_FACE ( 'NONE', ( #7402 ), #3511, .T. ) ;
#3286=VERTEX_POINT ( 'NONE', #2147 ) ;
#3313=CARTESIAN_POINT ( 'NONE',  ( 8.000000000000117240, -1.110223024625156540E-13, -8.400000000000018119 ) ) ;
#3326=AXIS2_PLACEMENT_3D ( 'NONE', #2552, #7861, #2462 ) ;
#3339=EDGE_LOOP ( 'NONE', ( #7406, #4421, #1814 ) ) ;
#3346=EDGE_CURVE ( 'NONE', #2011, #2131, #1840, .T. ) ;
#3348=VERTEX_POINT ( 'NONE', #3771 ) ;
#3349=FACE_OUTER_BOUND ( 'NONE', #1586, .T. ) ;
#3376=CARTESIAN_POINT ( 'NONE',  ( 0.000000000000000000, 0.000000000000000000, 0.000000000000000000 ) ) ;
#3382=CARTESIAN_POINT ( 'NONE',  ( -7.999999999999894307, 3.115336682266907964, -0.3193931313914263881 ) ) ;
#3398=CARTESIAN_POINT ( 'NONE',  ( -7.999999999999888978, -1.555946510856243581, -8.332911297836714581 ) ) ;
#3436=CARTESIAN_POINT ( 'NONE',  ( 7.345652830558639046, -4.996589667937789692, -7.903584543331145795 ) ) ;
#3443=CARTESIAN_POINT ( 'NONE',  ( 2.220446049250313081E-13, 9.237604307034075646, 0.000000000000000000 ) ) ;
#3454=EDGE_CURVE ( 'NONE', #3046, #3235, #924, .T. ) ;
#3455=SHAPE_REPRESENTATION ( 'hex nut style 1_am_B18.2.4.1M - Hex nut, Style 1,  M10 x 1.5, with 16mm WAF --D-N', ( #7563 ), #7435 ) ;
#3464=EDGE_LOOP ( 'NONE', ( #4377, #7954, #2106, #4854, #4969, #5551 ) ) ;
#3489=VERTEX_POINT ( 'NONE', #2068 ) ;
#3511=CONICAL_SURFACE ( 'NONE', #5330, 8.000000000000007105, 1.047197551196597631 ) ;
#3512=DIRECTION ( 'NONE',  ( 1.000000000000000000, 0.000000000000000000, 0.000000000000000000 ) ) ;
#3515=AXIS2_PLACEMENT_3D ( 'NONE', #3376, #2075, #3896 ) ;
#3535=PLANE ( 'NONE',  #3601 ) ;
#3543=FACE_OUTER_BOUND ( 'NONE', #5596, .T. ) ;
#3563=ORIENTED_EDGE ( 'NONE', *, *, #6051, .F. ) ;
#3590=EDGE_CURVE ( 'NONE', #3348, #3489, #589, .T. ) ;
#3598=CARTESIAN_POINT ( 'NONE',  ( 2.220446049250313081E-13, 9.237604307034075646, -8.400000000000018119 ) ) ;
#3600=EDGE_LOOP ( 'NONE', ( #6309, #6652, #1548 ) ) ;
#3601=AXIS2_PLACEMENT_3D ( 'NONE', #6849, #8319, #2341 ) ;
#3616=VECTOR ( 'NONE', #7905, 1000.000000000000000 ) ;
#3629=AXIS2_PLACEMENT_3D ( 'NONE', #1662, #4455, #5706 ) ;
#3660=ORIENTED_EDGE ( 'NONE', *, *, #5716, .F. ) ;
#3669=ORIENTED_EDGE ( 'NONE', *, *, #8470, .F. ) ;
#3677=CARTESIAN_POINT ( 'NONE',  ( 7.999999999999674039, -4.618802153517231446, -0.7145311798163467287 ) ) ;
#3690=EDGE_CURVE ( 'NONE', #3935, #2608, #1177, .T. ) ;
#3704=CARTESIAN_POINT ( 'NONE',  ( 4.000000000000225597, -6.928203230275542523, 0.000000000000000000 ) ) ;
#3709=EDGE_CURVE ( 'NONE', #5809, #3749, #2415, .T. ) ;
#3742=EDGE_CURVE ( 'NONE', #3286, #650, #1710, .T. ) ;
#3744=VERTEX_POINT ( 'NONE', #3313 ) ;
#3746=FACE_OUTER_BOUND ( 'NONE', #3464, .T. ) ;
#3747=VECTOR ( 'NONE', #6661, 1000.000000000000000 ) ;
#3749=VERTEX_POINT ( 'NONE', #34 ) ;
#3761=CARTESIAN_POINT ( 'NONE',  ( 0.000000000000000000, 0.000000000000000000, -8.400000000000018119 ) ) ;
#3771=CARTESIAN_POINT ( 'NONE',  ( 5.080504117408889186, 2.106769544347817824, -8.400000000000018119 ) ) ;
#3775=AXIS2_PLACEMENT_3D ( 'NONE', #1695, #4409, #6300 ) ;
#3779=CARTESIAN_POINT ( 'NONE',  ( -8.000000000000007105, -4.618802153517065356, -7.685468820183672278 ) ) ;
#3786=CARTESIAN_POINT ( 'NONE',  ( 2.309976723937862797, -7.903938623647071005, -0.1306530452039634804 ) ) ;
#3880=CONICAL_SURFACE ( 'NONE', #3056, 8.000000000000007105, 1.047197551196597631 ) ;
#3885=AXIS2_PLACEMENT_3D ( 'NONE', #6176, #2932, #7679 ) ;
#3890=ORIENTED_EDGE ( 'NONE', *, *, #5716, .T. ) ;
#3891=CARTESIAN_POINT ( 'NONE',  ( 5.355005115540952154, 6.145890662064715571, -8.317753204360256447 ) ) ;
#3892=CIRCLE ( 'NONE', #3629, 8.000000000000007105 ) ;
#3896=DIRECTION ( 'NONE',  ( 1.000000000000000000, 8.881784197001244435E-16, 0.000000000000000000 ) ) ;
#3905=CARTESIAN_POINT ( 'NONE',  ( -5.354491962338047806, 6.146186931204369763, -0.06809871960538080304 ) ) ;
#3919=DIRECTION ( 'NONE',  ( -1.000000000000000000, -8.881784197001244435E-16, 0.000000000000000000 ) ) ;
#3923=VECTOR ( 'NONE', #7843, 1000.000000000000000 ) ;
#3935=VERTEX_POINT ( 'NONE', #676 ) ;
#3937=CARTESIAN_POINT ( 'NONE',  ( 4.680456609904013909, 6.535341423375667702, -8.383111142572204244 ) ) ;
#3950=DIRECTION ( 'NONE',  ( 0.5000000000000035527, 0.8660254037844365982, 0.000000000000000000 ) ) ;
#3958=CARTESIAN_POINT ( 'NONE',  ( -4.681481898396918417, 6.534749472788111468, 4.815212898551246568E-14 ) ) ;
#3959=CARTESIAN_POINT ( 'NONE',  ( 2.644994884459374695, -7.710515798486562211, -8.317753204360146313 ) ) ;
#3962=PRODUCT_DEFINITION_FORMATION_WITH_SPECIFIED_SOURCE ( 'ANY', '', #5872, .NOT_KNOWN. ) ;
#3992=FACE_OUTER_BOUND ( 'NONE', #3600, .T. ) ;
#4002=CARTESIAN_POINT ( 'NONE',  ( -7.999999999999892530, -0.7805016046292091447, -8.400000000000073186 ) ) ;
#4011=ORIENTED_EDGE ( 'NONE', *, *, #3590, .F. ) ;
#4017=VECTOR ( 'NONE', #7309, 1000.000000000000000 ) ;
#4020=VECTOR ( 'NONE', #8168, 1000.000000000000000 ) ;
#4035=EDGE_CURVE ( 'NONE', #5809, #2338, #1743, .T. ) ;
#4039=DIRECTION ( 'NONE',  ( 0.000000000000000000, 0.000000000000000000, 1.000000000000000000 ) ) ;
#4057=ORIENTED_EDGE ( 'NONE', *, *, #1268, .T. ) ;
#4063=CYLINDRICAL_SURFACE ( 'NONE', #986, 5.500000000000023981 ) ;
#4073=ADVANCED_FACE ( 'NONE', ( #4246, #1538 ), #2123, .T. ) ;
#4095=CARTESIAN_POINT ( 'NONE',  ( 0.000000000000000000, 0.000000000000000000, 0.000000000000000000 ) ) ;
#4099=ORIENTED_EDGE ( 'NONE', *, *, #6939, .F. ) ;
#4114=ADVANCED_FACE ( 'NONE', ( #7428 ), #2070, .T. ) ;
#4117=EDGE_LOOP ( 'NONE', ( #6609, #7313, #1103 ) ) ;
#4125=CARTESIAN_POINT ( 'NONE',  ( -7.999999999999896083, 3.871967595402032725, -0.4989386132323781475 ) ) ;
#4128=CARTESIAN_POINT ( 'NONE',  ( -7.347286611336965478, -4.995646404165273502, -0.4969600502617496640 ) ) ;
#4145=DIRECTION ( 'NONE',  ( -1.000000000000000000, -8.881784197001244435E-16, 0.000000000000000000 ) ) ;
#4158=B_SPLINE_CURVE_WITH_KNOTS ( 'NONE', 3,
 ( #3142, #2487, #408, #2316, #5746, #5058 ),
 .UNSPECIFIED., .F., .F.,
 ( 4, 2, 4 ),
 ( 2.380731635918682947E-07, 0.002336973833157848703, 0.004673709593152105407 ),
 .UNSPECIFIED. ) ;
#4163=( NAMED_UNIT ( * ) SI_UNIT ( $, .STERADIAN. ) SOLID_ANGLE_UNIT ( ) );
#4171=ORIENTED_EDGE ( 'NONE', *, *, #5073, .F. ) ;
#4182=DIRECTION ( 'NONE',  ( 0.000000000000000000, 0.000000000000000000, -1.000000000000000000 ) ) ;
#4203=CARTESIAN_POINT ( 'NONE',  ( 0.000000000000000000, 0.000000000000000000, 0.000000000000000000 ) ) ;
#4205=AXIS2_PLACEMENT_3D ( 'NONE', #1460, #6222, #188 ) ;
#4225=AXIS2_PLACEMENT_3D ( 'NONE', #1739, #6295, #6451 ) ;
#4246=FACE_BOUND ( 'NONE', #1160, .T. ) ;
#4268=ORIENTED_EDGE ( 'NONE', *, *, #3709, .F. ) ;
#4271=ORIENTED_EDGE ( 'NONE', *, *, #3346, .F. ) ;
#4274=CARTESIAN_POINT ( 'NONE',  ( 2.645508037661955303, 7.710219529346674427, -8.331901280394536258 ) ) ;
#4327=ADVANCED_FACE ( 'NONE', ( #788 ), #7273, .T. ) ;
#4328=DIRECTION ( 'NONE',  ( 0.000000000000000000, 0.000000000000000000, 1.000000000000000000 ) ) ;
#4367=ORIENTED_EDGE ( 'NONE', *, *, #6937, .F. ) ;
#4368=DIRECTION ( 'NONE',  ( -1.000000000000000000, -8.881784197001244435E-16, 0.000000000000000000 ) ) ;
#4377=ORIENTED_EDGE ( 'NONE', *, *, #6246, .F. ) ;
#4409=DIRECTION ( 'NONE',  ( 0.000000000000000000, 0.000000000000000000, 1.000000000000000000 ) ) ;
#4421=ORIENTED_EDGE ( 'NONE', *, *, #8140, .T. ) ;
#4434=EDGE_CURVE ( 'NONE', #3744, #5809, #1703, .T. ) ;
#4449=AXIS2_PLACEMENT_3D ( 'NONE', #3761, #6420, #453 ) ;
#4452=PRODUCT_CONTEXT ( 'NONE', #6868, 'mechanical' ) ;
#4455=DIRECTION ( 'NONE',  ( -0.000000000000000000, -0.000000000000000000, 1.000000000000000000 ) ) ;
#4459=CARTESIAN_POINT ( 'NONE',  ( -0.6527133886628254666, 8.860760056385792893, -0.4969600502617717019 ) ) ;
#4472=DIRECTION ( 'NONE',  ( -1.000000000000000000, -8.881784197001244435E-16, 0.000000000000000000 ) ) ;
#4516=CONICAL_SURFACE ( 'NONE', #763, 8.000000000000007105, 1.047197551196597631 ) ;
#4540=VECTOR ( 'NONE', #1382, 1000.000000000000000 ) ;
#4559=CARTESIAN_POINT ( 'NONE',  ( 0.000000000000000000, 0.000000000000000000, -8.400000000000018119 ) ) ;
#4582=ORIENTED_EDGE ( 'NONE', *, *, #1266, .F. ) ;
#4586=ADVANCED_BREP_SHAPE_REPRESENTATION ( '', ( #40, #7563 ), #7435 ) ;
#4595=ADVANCED_FACE ( 'NONE', ( #5415 ), #1571, .T. ) ;
#4619=CARTESIAN_POINT ( 'NONE',  ( -7.999999999999888978, -3.098204225878262719, -8.084209322808188602 ) ) ;
#4621=CARTESIAN_POINT ( 'NONE',  ( 0.000000000000000000, 0.000000000000000000, 0.000000000000000000 ) ) ;
#4626=CARTESIAN_POINT ( 'NONE',  ( 0.000000000000000000, 0.000000000000000000, -8.400000000000018119 ) ) ;
#4660=CARTESIAN_POINT ( 'NONE',  ( 0.6527133886632227044, -8.860760056385986516, -7.903039949738120740 ) ) ;
#4693=DIRECTION ( 'NONE',  ( -1.000000000000000000, -8.881784197001244435E-16, 0.000000000000000000 ) ) ;
#4702=ADVANCED_FACE ( 'NONE', ( #967 ), #2394, .F. ) ;
#4706=CARTESIAN_POINT ( 'NONE',  ( -8.000000000000117240, -1.110223024625156540E-13, 0.000000000000000000 ) ) ;
#4715=ORIENTED_EDGE ( 'NONE', *, *, #3346, .T. ) ;
#4721=CARTESIAN_POINT ( 'NONE',  ( 0.6543471694414042528, 8.859816792613671055, -0.4964154566688170900 ) ) ;
#4727=DIRECTION ( 'NONE',  ( -1.000000000000000000, -8.881784197001244435E-16, -0.000000000000000000 ) ) ;
#4751=ORIENTED_EDGE ( 'NONE', *, *, #5373, .T. ) ;
#4753=ORIENTED_EDGE ( 'NONE', *, *, #2038, .F. ) ;
#4786=CARTESIAN_POINT ( 'NONE',  ( -6.689127551062022725, -5.375634714784609081, -0.3173508448886571132 ) ) ;
#4816=DIRECTION ( 'NONE',  ( 0.000000000000000000, 0.000000000000000000, -1.000000000000000000 ) ) ;
#4820=CARTESIAN_POINT ( 'NONE',  ( 7.999999999999674039, -4.618802153517231446, -7.685468820183672278 ) ) ;
#4823=( LENGTH_UNIT ( ) NAMED_UNIT ( * ) SI_UNIT ( .MILLI., .METRE. ) );
#4854=ORIENTED_EDGE ( 'NONE', *, *, #7775, .T. ) ;
#4906=DIRECTION ( 'NONE',  ( 1.000000000000000000, 8.881784197001244435E-16, 0.000000000000000000 ) ) ;
#4914=DIRECTION ( 'NONE',  ( 0.5000000000000029976, -0.8660254037844370423, 0.000000000000000000 ) ) ;
#4949=CARTESIAN_POINT ( 'NONE',  ( 4.000000000000225597, -6.928203230275542523, -8.400000000000018119 ) ) ;
#4956=ORIENTED_EDGE ( 'NONE', *, *, #4434, .F. ) ;
#4964=ORIENTED_EDGE ( 'NONE', *, *, #6889, .T. ) ;
#4969=ORIENTED_EDGE ( 'NONE', *, *, #5664, .T. ) ;
#4970=DIRECTION ( 'NONE',  ( 0.000000000000000000, 0.000000000000000000, -1.000000000000000000 ) ) ;
#4971=DIRECTION ( 'NONE',  ( 1.000000000000000000, 8.881784197001244435E-16, 0.000000000000000000 ) ) ;
#4991=CARTESIAN_POINT ( 'NONE',  ( 0.000000000000000000, -9.237604307034018802, -0.7145311798163467287 ) ) ;
#5015=CIRCLE ( 'NONE', #6421, 8.000000000000007105 ) ;
#5019=ADVANCED_FACE ( 'NONE', ( #3992 ), #1075, .T. ) ;
#5040=ADVANCED_FACE ( 'NONE', ( #2033 ), #1242, .T. ) ;
#5058=CARTESIAN_POINT ( 'NONE',  ( -3.999999999999892530, 6.928203230275431501, -8.400000000000018119 ) ) ;
#5064=DIRECTION ( 'NONE',  ( 0.000000000000000000, 0.000000000000000000, 1.000000000000000000 ) ) ;
#5073=EDGE_CURVE ( 'NONE', #2801, #3286, #3168, .T. ) ;
#5077=CARTESIAN_POINT ( 'NONE',  ( 2.220446049250313081E-13, 9.237604307034075646, -7.685468820183672278 ) ) ;
#5083=ORIENTED_EDGE ( 'NONE', *, *, #402, .F. ) ;
#5091=CARTESIAN_POINT ( 'NONE',  ( 8.000000000000238032, -3.867591403079324142, -0.4976753153247437944 ) ) ;
#5125=FACE_OUTER_BOUND ( 'NONE', #8365, .T. ) ;
#5140=DIRECTION ( 'NONE',  ( -1.000000000000000000, -8.881784197001244435E-16, 0.000000000000000000 ) ) ;
#5149=CARTESIAN_POINT ( 'NONE',  ( 2.220446049250313081E-13, 9.237604307034075646, -8.400000000000018119 ) ) ;
#5158=CARTESIAN_POINT ( 'NONE',  ( -1.313474075707240729, -8.479269695850863542, -0.3167204509598423590 ) ) ;
#5168=CONICAL_SURFACE ( 'NONE', #6563, 8.000000000000007105, 1.047197551196597631 ) ;
#5169=PLANE ( 'NONE',  #1163 ) ;
#5179=EDGE_CURVE ( 'NONE', #1467, #3109, #7367, .T. ) ;
#5194=CARTESIAN_POINT ( 'NONE',  ( 4.000000000000225597, -6.928203230275542523, -8.400000000000018119 ) ) ;
#5202=ORIENTED_EDGE ( 'NONE', *, *, #5179, .T. ) ;
#5217=CARTESIAN_POINT ( 'NONE',  ( 8.000000000000234479, -1.555946510856276666, -8.332911297836512077 ) ) ;
#5226=CARTESIAN_POINT ( 'NONE',  ( -2.645508037661928213, -7.710219529346594491, -8.331901280394589548 ) ) ;
#5239=ORIENTED_EDGE ( 'NONE', *, *, #47, .T. ) ;
#5251=CARTESIAN_POINT ( 'NONE',  ( -7.999999999999896083, 4.618802153516899267, -8.400000000000018119 ) ) ;
#5266=ORIENTED_EDGE ( 'NONE', *, *, #8470, .T. ) ;
#5270=CARTESIAN_POINT ( 'NONE',  ( 8.000000000000238032, -3.098204225878349760, -0.3157906771920377387 ) ) ;
#5290=AXIS2_PLACEMENT_3D ( 'NONE', #3443, #2702, #5494 ) ;
#5302=ORIENTED_EDGE ( 'NONE', *, *, #402, .T. ) ;
#5315=CARTESIAN_POINT ( 'NONE',  ( 0.000000000000000000, -9.237604307034018802, -7.685468820183672278 ) ) ;
#5330=AXIS2_PLACEMENT_3D ( 'NONE', #4095, #1072, #6762 ) ;
#5353=CARTESIAN_POINT ( 'NONE',  ( 8.000000000000117240, -1.110223024625156540E-13, -8.400000000000018119 ) ) ;
#5365=CIRCLE ( 'NONE', #2721, 5.500000000000023981 ) ;
#5373=EDGE_CURVE ( 'NONE', #3489, #3348, #5365, .T. ) ;
#5391=ADVANCED_FACE ( 'NONE', ( #1777 ), #4516, .T. ) ;
#5393=ORIENTED_EDGE ( 'NONE', *, *, #6246, .T. ) ;
#5395=CARTESIAN_POINT ( 'NONE',  ( 8.000000000000117240, 4.618802153517009401, -0.7145311798163467287 ) ) ;
#5396=ADVANCED_FACE ( 'NONE', ( #5125 ), #1874, .T. ) ;
#5398=CARTESIAN_POINT ( 'NONE',  ( 0.000000000000000000, -9.237604307034018802, -7.685468820183672278 ) ) ;
#5399=AXIS2_PLACEMENT_3D ( 'NONE', #7216, #7342, #6559 ) ;
#5404=CARTESIAN_POINT ( 'NONE',  ( 2.220446049250313081E-13, 9.237604307034075646, -0.7145311798163467287 ) ) ;
#5412=CARTESIAN_POINT ( 'NONE',  ( 0.000000000000000000, 0.000000000000000000, 0.000000000000000000 ) ) ;
#5415=FACE_OUTER_BOUND ( 'NONE', #8304, .T. ) ;
#5435=VECTOR ( 'NONE', #5064, 1000.000000000000000 ) ;
#5448=CARTESIAN_POINT ( 'NONE',  ( -7.999999999999894307, 3.115336682266945711, -8.080606868608583682 ) ) ;
#5450=CARTESIAN_POINT ( 'NONE',  ( 1.310872448938211532, -8.480771745766629621, -8.082649155111216288 ) ) ;
#5452=CARTESIAN_POINT ( 'NONE',  ( -7.999999999999890754, -0.7805016046292094778, 5.627856308147021051E-14 ) ) ;
#5457=DIRECTION ( 'NONE',  ( -1.000000000000000000, -1.421085471520200372E-14, 0.000000000000000000 ) ) ;
#5494=DIRECTION ( 'NONE',  ( -1.000000000000000000, -8.881784197001244435E-16, -0.000000000000000000 ) ) ;
#5504=CARTESIAN_POINT ( 'NONE',  ( -7.999999999999890754, -3.867591403079264190, -7.902324684675469335 ) ) ;
#5511=ADVANCED_FACE ( 'NONE', ( #6649 ), #2689, .T. ) ;
#5514=CARTESIAN_POINT ( 'NONE',  ( -8.000000000000007105, -4.618802153517065356, -0.7145311798163467287 ) ) ;
#5521=CARTESIAN_POINT ( 'NONE',  ( -7.999999999999785061, -4.618802153517121312, -8.400000000000018119 ) ) ;
#5550=DIRECTION ( 'NONE',  ( -0.9237280213470678847, -0.3830490080632384942, 0.000000000000000000 ) ) ;
#5551=ORIENTED_EDGE ( 'NONE', *, *, #455, .F. ) ;
#5570=CARTESIAN_POINT ( 'NONE',  ( -3.999999999999892530, 6.928203230275431501, 0.000000000000000000 ) ) ;
#5589=B_SPLINE_CURVE_WITH_KNOTS ( 'NONE', 3,
 ( #3010, #5091, #5270, #7886, #1877, #1217 ),
 .UNSPECIFIED., .F., .F.,
 ( 4, 2, 4 ),
 ( 0.008240550023493446036, 0.01057684187039402771, 0.01291313371729461111 ),
 .UNSPECIFIED. ) ;
#5596=EDGE_LOOP ( 'NONE', ( #4367, #8542, #7759, #2188 ) ) ;
#5626=CARTESIAN_POINT ( 'NONE',  ( 4.681481898397195529, -6.534749472788381475, -8.399999999999842260 ) ) ;
#5643=EDGE_CURVE ( 'NONE', #3935, #3744, #54, .T. ) ;
#5664=EDGE_CURVE ( 'NONE', #2338, #7258, #2648, .T. ) ;
#5706=DIRECTION ( 'NONE',  ( -1.000000000000000000, -8.881784197001244435E-16, 0.000000000000000000 ) ) ;
#5712=ORIENTED_EDGE ( 'NONE', *, *, #3454, .T. ) ;
#5716=EDGE_CURVE ( 'NONE', #2801, #7042, #2343, .T. ) ;
#5720=DIRECTION ( 'NONE',  ( -1.000000000000000000, -8.881784197001244435E-16, 0.000000000000000000 ) ) ;
#5726=PLANE ( 'NONE',  #6006 ) ;
#5746=CARTESIAN_POINT ( 'NONE',  ( -4.681481898396900654, 6.534749472788120350, -8.400000000000067857 ) ) ;
#5760=DIRECTION ( 'NONE',  ( 0.000000000000000000, 0.000000000000000000, -1.000000000000000000 ) ) ;
#5765=CARTESIAN_POINT ( 'NONE',  ( -3.999999999999892530, 6.928203230275431501, -8.400000000000018119 ) ) ;
#5809=VERTEX_POINT ( 'NONE', #2651 ) ;
#5818=CARTESIAN_POINT ( 'NONE',  ( 0.000000000000000000, 0.000000000000000000, 0.000000000000000000 ) ) ;
#5832=B_SPLINE_CURVE_WITH_KNOTS ( 'NONE', 3,
 ( #5970, #2079, #8045, #3382, #4125, #2817 ),
 .UNSPECIFIED., .F., .F.,
 ( 4, 2, 4 ),
 ( 0.01291313371729460764, 0.01525081363757309350, 0.01758849355785158108 ),
 .UNSPECIFIED. ) ;
#5842=CARTESIAN_POINT ( 'NONE',  ( -8.000000000000007105, -4.618802153517065356, -7.685468820183672278 ) ) ;
#5872=PRODUCT ( 'hex nut style 1_am_B18.2.4.1M - Hex nut, Style 1,  M10 x 1.5, with 16mm WAF --D-N', 'hex nut style 1_am_B18.2.4.1M - Hex nut, Style 1,  M10 x 1.5, with 16mm WAF --D-N', '', ( #4452 ) ) ;
#5884=CARTESIAN_POINT ( 'NONE',  ( 6.689127551062092891, 5.375634714784657930, -8.082649155111312211 ) ) ;
#5886=CARTESIAN_POINT ( 'NONE',  ( 2.220446049250313081E-13, -9.237604307034242623, -8.400000000000018119 ) ) ;
#5897=ADVANCED_FACE ( 'NONE', ( #6362 ), #7661, .T. ) ;
#5903=VERTEX_POINT ( 'NONE', #5842 ) ;
#5970=CARTESIAN_POINT ( 'NONE',  ( -8.000000000000117240, -1.110223024625156540E-13, 0.000000000000000000 ) ) ;
#5982=ADVANCED_FACE ( 'NONE', ( #7860 ), #5168, .T. ) ;
#5983=CARTESIAN_POINT ( 'NONE',  ( 6.686525924292749501, -5.377136764700527927, -0.3167204509599568785 ) ) ;
#6002=CARTESIAN_POINT ( 'NONE',  ( 2.645508037661955303, 7.710219529346675316, -0.06809871960547979330 ) ) ;
#6006=AXIS2_PLACEMENT_3D ( 'NONE', #8359, #4914, #348 ) ;
#6013=LINE ( 'NONE', #5251, #3616 ) ;
#6051=EDGE_CURVE ( 'NONE', #3105, #7042, #7298, .T. ) ;
#6080=ORIENTED_EDGE ( 'NONE', *, *, #1266, .T. ) ;
#6082=ORIENTED_EDGE ( 'NONE', *, *, #2607, .F. ) ;
#6107=CARTESIAN_POINT ( 'NONE',  ( -7.345652830558694113, 4.996589667937325174, -0.4964154566687435377 ) ) ;
#6150=CARTESIAN_POINT ( 'NONE',  ( -4.339467034331259576, -6.732211846623360252, -9.205130554286108935E-16 ) ) ;
#6176=CARTESIAN_POINT ( 'NONE',  ( 0.000000000000000000, 0.000000000000000000, 0.000000000000000000 ) ) ;
#6192=CARTESIAN_POINT ( 'NONE',  ( 7.999999999999674039, -4.618802153517231446, -7.685468820183672278 ) ) ;
#6204=CARTESIAN_POINT ( 'NONE',  ( 8.000000000000117240, -1.110223024625156540E-13, 0.000000000000000000 ) ) ;
#6222=DIRECTION ( 'NONE',  ( -0.5000000000000041078, 0.8660254037844363761, 0.000000000000000000 ) ) ;
#6226=EDGE_CURVE ( 'NONE', #902, #5809, #1012, .T. ) ;
#6233=DIRECTION ( 'NONE',  ( 0.000000000000000000, 0.000000000000000000, 1.000000000000000000 ) ) ;
#6237=ORIENTED_EDGE ( 'NONE', *, *, #2607, .T. ) ;
#6246=EDGE_CURVE ( 'NONE', #2608, #2278, #5589, .T. ) ;
#6262=CIRCLE ( 'NONE', #2486, 5.500000000000023981 ) ;
#6295=DIRECTION ( 'NONE',  ( 0.000000000000000000, 0.000000000000000000, 1.000000000000000000 ) ) ;
#6300=DIRECTION ( 'NONE',  ( 1.000000000000000000, 8.881784197001244435E-16, 0.000000000000000000 ) ) ;
#6309=ORIENTED_EDGE ( 'NONE', *, *, #559, .T. ) ;
#6316=ORIENTED_EDGE ( 'NONE', *, *, #7775, .F. ) ;
#6342=CARTESIAN_POINT ( 'NONE',  ( 7.999999999999674039, -4.618802153517231446, -0.7145311798163467287 ) ) ;
#6356=ORIENTED_EDGE ( 'NONE', *, *, #6051, .T. ) ;
#6362=FACE_OUTER_BOUND ( 'NONE', #4117, .T. ) ;
#6378=DIRECTION ( 'NONE',  ( 0.000000000000000000, 0.000000000000000000, -1.000000000000000000 ) ) ;
#6380=CARTESIAN_POINT ( 'NONE',  ( 8.000000000000117240, -1.110223024625156540E-13, 0.000000000000000000 ) ) ;
#6382=FACE_OUTER_BOUND ( 'NONE', #785, .T. ) ;
#6383=FACE_OUTER_BOUND ( 'NONE', #1941, .T. ) ;
#6400=CARTESIAN_POINT ( 'NONE',  ( -5.690023276062435187, -5.952467836904131282, -8.269346954796199967 ) ) ;
#6405=EDGE_CURVE ( 'NONE', #8505, #2011, #7007, .T. ) ;
#6410=DIRECTION ( 'NONE',  ( 0.000000000000000000, 0.000000000000000000, 1.000000000000000000 ) ) ;
#6420=DIRECTION ( 'NONE',  ( -0.000000000000000000, -0.000000000000000000, 1.000000000000000000 ) ) ;
#6421=AXIS2_PLACEMENT_3D ( 'NONE', #8289, #4970, #4368 ) ;
#6451=DIRECTION ( 'NONE',  ( -0.9237280213470678847, -0.3830490080632384942, 0.000000000000000000 ) ) ;
#6467=ORIENTED_EDGE ( 'NONE', *, *, #424, .T. ) ;
#6474=DIRECTION ( 'NONE',  ( -0.5000000000000033307, -0.8660254037844367092, 0.000000000000000000 ) ) ;
#6518=CONICAL_SURFACE ( 'NONE', #2270, 8.000000000000007105, 1.047197551196597631 ) ;
#6541=ADVANCED_FACE ( 'NONE', ( #8151 ), #3535, .T. ) ;
#6546=VERTEX_POINT ( 'NONE', #215 ) ;
#6550=CARTESIAN_POINT ( 'NONE',  ( 8.000000000000117240, 4.618802153517009401, -7.685468820183672278 ) ) ;
#6556=CARTESIAN_POINT ( 'NONE',  ( -8.000000000000117240, -1.110223024625156540E-13, -8.400000000000018119 ) ) ;
#6559=DIRECTION ( 'NONE',  ( -1.000000000000000000, -8.881784197001244435E-16, 0.000000000000000000 ) ) ;
#6563=AXIS2_PLACEMENT_3D ( 'NONE', #1982, #8508, #544 ) ;
#6593=CARTESIAN_POINT ( 'NONE',  ( 8.000000000000117240, -1.110223024625156540E-13, -8.400000000000018119 ) ) ;
#6598=ORIENTED_EDGE ( 'NONE', *, *, #6405, .F. ) ;
#6609=ORIENTED_EDGE ( 'NONE', *, *, #424, .F. ) ;
#6616=CARTESIAN_POINT ( 'NONE',  ( -7.999999999999894307, 1.572549600175527917, -8.331055444744958294 ) ) ;
#6622=CARTESIAN_POINT ( 'NONE',  ( 0.000000000000000000, 0.000000000000000000, 0.000000000000000000 ) ) ;
#6638=AXIS2_PLACEMENT_3D ( 'NONE', #1292, #3950, #1990 ) ;
#6649=FACE_OUTER_BOUND ( 'NONE', #6707, .T. ) ;
#6652=ORIENTED_EDGE ( 'NONE', *, *, #2038, .T. ) ;
#6653=CARTESIAN_POINT ( 'NONE',  ( 4.680456609904014798, 6.535341423375668590, -0.01688885742781526603 ) ) ;
#6659=CARTESIAN_POINT ( 'NONE',  ( -7.999999999999896083, 4.618802153516899267, -0.7145311798163467287 ) ) ;
#6661=DIRECTION ( 'NONE',  ( 0.000000000000000000, 0.000000000000000000, 1.000000000000000000 ) ) ;
#6684=CARTESIAN_POINT ( 'NONE',  ( 8.000000000000234479, 1.572549600175502604, -8.331055444744771776 ) ) ;
#6693=CARTESIAN_POINT ( 'NONE',  ( -4.000000000000114575, -6.928203230275542523, 0.000000000000000000 ) ) ;
#6707=EDGE_LOOP ( 'NONE', ( #6356, #5302, #8313, #393, #8026, #3068 ) ) ;
#6752=CARTESIAN_POINT ( 'NONE',  ( -4.000000000000114575, -6.928203230275542523, 0.000000000000000000 ) ) ;
#6762=DIRECTION ( 'NONE',  ( -1.000000000000000000, -8.881784197001244435E-16, 0.000000000000000000 ) ) ;
#6795=CARTESIAN_POINT ( 'NONE',  ( 4.339467034331236484, 6.732211846623466833, -4.488406411676854877E-14 ) ) ;
#6799=CARTESIAN_POINT ( 'NONE',  ( 0.000000000000000000, 0.000000000000000000, 0.000000000000000000 ) ) ;
#6814=CARTESIAN_POINT ( 'NONE',  ( 1.310872448938211754, -8.480771745766627845, -0.3173508448888029410 ) ) ;
#6817=APPLICATION_CONTEXT ( 'automotive_design' ) ;
#6826=ORIENTED_EDGE ( 'NONE', *, *, #3454, .F. ) ;
#6834=UNCERTAINTY_MEASURE_WITH_UNIT (LENGTH_MEASURE( 1.000000000000000082E-05 ), #4823, 'distance_accuracy_value', 'NONE');
#6843=EDGE_LOOP ( 'NONE', ( #8245, #4057, #5712, #293, #3669, #1128 ) ) ;
#6849=CARTESIAN_POINT ( 'NONE',  ( -7.999999999999896083, 4.618802153516899267, -8.400000000000018119 ) ) ;
#6857=ORIENTED_EDGE ( 'NONE', *, *, #3742, .T. ) ;
#6868=APPLICATION_CONTEXT ( 'automotive_design' ) ;
#6878=CARTESIAN_POINT ( 'NONE',  ( 0.000000000000000000, 0.000000000000000000, -8.400000000000018119 ) ) ;
#6885=CARTESIAN_POINT ( 'NONE',  ( -7.999999999999896083, 4.618802153516899267, -0.7145311798163467287 ) ) ;
#6887=EDGE_CURVE ( 'NONE', #3489, #3109, #7264, .T. ) ;
#6889=EDGE_CURVE ( 'NONE', #2131, #3105, #1184, .T. ) ;
#6917=EDGE_LOOP ( 'NONE', ( #4011, #8326, #5202, #1252 ) ) ;
#6919=EDGE_LOOP ( 'NONE', ( #3039, #1973, #1020, #191, #3218, #850 ) ) ;
#6922=CARTESIAN_POINT ( 'NONE',  ( -5.690023276062435187, -5.952467836904131282, -0.1306530452038156265 ) ) ;
#6937=EDGE_CURVE ( 'NONE', #3348, #1467, #2140, .T. ) ;
#6939=EDGE_CURVE ( 'NONE', #3109, #1467, #6262, .T. ) ;
#6941=CARTESIAN_POINT ( 'NONE',  ( 8.000000000000117240, 4.618802153517009401, -7.685468820183672278 ) ) ;
#6950=ORIENTED_EDGE ( 'NONE', *, *, #3690, .T. ) ;
#6958=AXIS2_PLACEMENT_3D ( 'NONE', #6622, #1138, #5140 ) ;
#7007=CIRCLE ( 'NONE', #2686, 8.000000000000007105 ) ;
#7042=VERTEX_POINT ( 'NONE', #4991 ) ;
#7049=CARTESIAN_POINT ( 'NONE',  ( -5.355005115540942384, -6.145890662064630305, -8.317753204360297303 ) ) ;
#7059=EDGE_LOOP ( 'NONE', ( #1884, #5083, #3660 ) ) ;
#7069=CARTESIAN_POINT ( 'NONE',  ( 0.000000000000000000, 0.000000000000000000, -8.400000000000018119 ) ) ;
#7095=PRODUCT_DEFINITION_SHAPE ( 'NONE', 'NONE',  #3008 ) ;
#7121=CARTESIAN_POINT ( 'NONE',  ( 2.220446049250313081E-13, 9.237604307034075646, -0.7145311798163467287 ) ) ;
#7128=CARTESIAN_POINT ( 'NONE',  ( -4.339467034331259576, -6.732211846623360252, -8.400000000000018119 ) ) ;
#7165=CARTESIAN_POINT ( 'NONE',  ( 4.339467034331238260, 6.732211846623467721, -8.399999999999973710 ) ) ;
#7182=ADVANCED_FACE ( 'NONE', ( #510 ), #414, .T. ) ;
#7198=EDGE_CURVE ( 'NONE', #2011, #5903, #8556, .T. ) ;
#7206=CARTESIAN_POINT ( 'NONE',  ( 7.347286611337071172, 4.995646404165302812, -7.903039949738208669 ) ) ;
#7209=DIRECTION ( 'NONE',  ( 0.000000000000000000, 0.000000000000000000, 1.000000000000000000 ) ) ;
#7216=CARTESIAN_POINT ( 'NONE',  ( 0.000000000000000000, 0.000000000000000000, 0.000000000000000000 ) ) ;
#7237=DIRECTION ( 'NONE',  ( -0.000000000000000000, -0.000000000000000000, 1.000000000000000000 ) ) ;
#7258=VERTEX_POINT ( 'NONE', #2688 ) ;
#7264=LINE ( 'NONE', #7964, #3747 ) ;
#7271=CARTESIAN_POINT ( 'NONE',  ( -8.000000000000117240, -1.110223024625156540E-13, -8.400000000000018119 ) ) ;
#7273=CONICAL_SURFACE ( 'NONE', #2538, 8.000000000000007105, 1.047197551196597631 ) ;
#7290=CARTESIAN_POINT ( 'NONE',  ( 3.318518101603052273, 7.321656987762953150, -5.096427837039673649E-14 ) ) ;
#7298=LINE ( 'NONE', #5886, #5 ) ;
#7309=DIRECTION ( 'NONE',  ( 0.000000000000000000, 0.000000000000000000, 1.000000000000000000 ) ) ;
#7313=ORIENTED_EDGE ( 'NONE', *, *, #455, .T. ) ;
#7316=DIRECTION ( 'NONE',  ( 1.000000000000000000, 8.881784197001244435E-16, 0.000000000000000000 ) ) ;
#7342=DIRECTION ( 'NONE',  ( 0.000000000000000000, 0.000000000000000000, -1.000000000000000000 ) ) ;
#7348=CARTESIAN_POINT ( 'NONE',  ( -7.999999999999785061, 4.618802153516954334, -7.685468820183672278 ) ) ;
#7354=CARTESIAN_POINT ( 'NONE',  ( -4.000000000000114575, -6.928203230275542523, -8.400000000000018119 ) ) ;
#7365=EDGE_CURVE ( 'NONE', #6546, #2856, #6013, .T. ) ;
#7367=CIRCLE ( 'NONE', #3885, 5.500000000000023981 ) ;
#7381=ORIENTED_EDGE ( 'NONE', *, *, #2561, .T. ) ;
#7402=FACE_OUTER_BOUND ( 'NONE', #3339, .T. ) ;
#7406=ORIENTED_EDGE ( 'NONE', *, *, #2988, .F. ) ;
#7410=AXIS2_PLACEMENT_3D ( 'NONE', #570, #3140, #7931 ) ;
#7427=AXIS2_PLACEMENT_3D ( 'NONE', #7972, #2005, #7316 ) ;
#7428=FACE_OUTER_BOUND ( 'NONE', #6843, .T. ) ;
#7435=( GEOMETRIC_REPRESENTATION_CONTEXT ( 3 ) GLOBAL_UNCERTAINTY_ASSIGNED_CONTEXT ( ( #446 ) ) GLOBAL_UNIT_ASSIGNED_CONTEXT ( ( #3151, #7897, #626 ) ) REPRESENTATION_CONTEXT ( 'NONE', 'WORKASPACE' ) );
#7443=CARTESIAN_POINT ( 'NONE',  ( 4.000000000000225597, -6.928203230275542523, 0.000000000000000000 ) ) ;
#7444=FACE_OUTER_BOUND ( 'NONE', #2362, .T. ) ;
#7446=CARTESIAN_POINT ( 'NONE',  ( 5.080504117408889186, 2.106769544347817824, 0.000000000000000000 ) ) ;
#7448=CARTESIAN_POINT ( 'NONE',  ( 5.080504117408895404, 2.106769544347820489, -8.401000000000047763 ) ) ;
#7477=CARTESIAN_POINT ( 'NONE',  ( 8.000000000000238032, -3.867591403079327250, -7.902324684675273936 ) ) ;
#7478=DIRECTION ( 'NONE',  ( 0.000000000000000000, 0.000000000000000000, 1.000000000000000000 ) ) ;
#7513=ORIENTED_EDGE ( 'NONE', *, *, #3709, .T. ) ;
#7522=ORIENTED_EDGE ( 'NONE', *, *, #3184, .T. ) ;
#7554=ORIENTED_EDGE ( 'NONE', *, *, #6889, .F. ) ;
#7563=AXIS2_PLACEMENT_3D ( 'NONE', #4203, #7478, #3512 ) ;
#7595=ORIENTED_EDGE ( 'NONE', *, *, #2988, .T. ) ;
#7600=ORIENTED_EDGE ( 'NONE', *, *, #7365, .F. ) ;
#7603=ORIENTED_EDGE ( 'NONE', *, *, #576, .F. ) ;
#7605=EDGE_CURVE ( 'NONE', #902, #3235, #532, .T. ) ;
#7612=B_SPLINE_CURVE_WITH_KNOTS ( 'NONE', 3,
 ( #6204, #8520, #8562, #1296, #2601, #5395 ),
 .UNSPECIFIED., .F., .F.,
 ( 4, 2, 4 ),
 ( 0.01291313371729461111, 0.01525081363757316288, 0.01758849355785171292 ),
 .UNSPECIFIED. ) ;
#7632=CARTESIAN_POINT ( 'NONE',  ( 4.681481898397195529, -6.534749472788381475, -1.776617725548004789E-13 ) ) ;
#7651=CARTESIAN_POINT ( 'NONE',  ( -8.000000000000117240, -1.110223024625156540E-13, 0.000000000000000000 ) ) ;
#7661=CONICAL_SURFACE ( 'NONE', #8235, 8.000000000000007105, 1.047197551196597631 ) ;
#7679=DIRECTION ( 'NONE',  ( -0.9237280213470678847, -0.3830490080632384942, 0.000000000000000000 ) ) ;
#7717=CARTESIAN_POINT ( 'NONE',  ( 5.354491962338240540, -6.146186931204690396, -0.06809871960559767123 ) ) ;
#7733=CARTESIAN_POINT ( 'NONE',  ( -0.6527133886628256887, 8.860760056385791117, -7.903039949738245085 ) ) ;
#7741=CARTESIAN_POINT ( 'NONE',  ( 3.319543390096325375, -7.321065037175607415, -0.01688885742793171801 ) ) ;
#7758=CARTESIAN_POINT ( 'NONE',  ( 4.000000000000225597, -6.928203230275542523, 0.000000000000000000 ) ) ;
#7759=ORIENTED_EDGE ( 'NONE', *, *, #6887, .T. ) ;
#7764=CARTESIAN_POINT ( 'NONE',  ( 0.000000000000000000, 0.000000000000000000, -8.400000000000018119 ) ) ;
#7775=EDGE_CURVE ( 'NONE', #3744, #2338, #2765, .T. ) ;
#7808=CARTESIAN_POINT ( 'NONE',  ( -3.999999999999892530, 6.928203230275431501, 0.000000000000000000 ) ) ;
#7815=CARTESIAN_POINT ( 'NONE',  ( -2.645508037661928213, -7.710219529346594491, -0.06809871960542769609 ) ) ;
#7824=EDGE_CURVE ( 'NONE', #3235, #1504, #2451, .T. ) ;
#7843=DIRECTION ( 'NONE',  ( 0.000000000000000000, 0.000000000000000000, 1.000000000000000000 ) ) ;
#7860=FACE_OUTER_BOUND ( 'NONE', #3025, .T. ) ;
#7861=DIRECTION ( 'NONE',  ( 0.000000000000000000, 0.000000000000000000, -1.000000000000000000 ) ) ;
#7881=CARTESIAN_POINT ( 'NONE',  ( -8.000000000000007105, -4.618802153517065356, -7.685468820183672278 ) ) ;
#7886=CARTESIAN_POINT ( 'NONE',  ( 8.000000000000234479, -1.555946510856281106, -0.06708870216350279470 ) ) ;
#7897=( NAMED_UNIT ( * ) PLANE_ANGLE_UNIT ( ) SI_UNIT ( $, .RADIAN. ) );
#7904=B_SPLINE_CURVE_WITH_KNOTS ( 'NONE', 3,
 ( #6659, #6107, #2778, #3905, #3958, #690 ),
 .UNSPECIFIED., .F., .F.,
 ( 4, 2, 4 ),
 ( 2.380731634700986265E-07, 0.002336973833157787988, 0.004673709593152105407 ),
 .UNSPECIFIED. ) ;
#7905=DIRECTION ( 'NONE',  ( 0.000000000000000000, 0.000000000000000000, 1.000000000000000000 ) ) ;
#7907=ORIENTED_EDGE ( 'NONE', *, *, #4434, .T. ) ;
#7931=DIRECTION ( 'NONE',  ( 0.9237280213470678847, 0.3830490080632384942, 0.000000000000000000 ) ) ;
#7954=ORIENTED_EDGE ( 'NONE', *, *, #3690, .F. ) ;
#7963=AXIS2_PLACEMENT_3D ( 'NONE', #3598, #4816, #4727 ) ;
#7964=CARTESIAN_POINT ( 'NONE',  ( -5.080504117408895404, -2.106769544347820933, -8.401000000000047763 ) ) ;
#7967=CARTESIAN_POINT ( 'NONE',  ( -7.999999999999890754, -1.555946510856244025, -0.06708870216330432845 ) ) ;
#7972=CARTESIAN_POINT ( 'NONE',  ( 0.000000000000000000, 0.000000000000000000, -8.400000000000018119 ) ) ;
#7999=DIRECTION ( 'NONE',  ( 0.8660254037844367092, -0.5000000000000033307, 0.000000000000000000 ) ) ;
#8013=B_SPLINE_CURVE_WITH_KNOTS ( 'NONE', 3,
 ( #1246, #2652, #6616, #5448, #604, #7348 ),
 .UNSPECIFIED., .F., .F.,
 ( 4, 2, 4 ),
 ( 0.01291313371729461111, 0.01525081363757312125, 0.01758849355785162966 ),
 .UNSPECIFIED. ) ;
#8015=CARTESIAN_POINT ( 'NONE',  ( -8.000000000000007105, -4.618802153517065356, -0.7145311798163467287 ) ) ;
#8023=CARTESIAN_POINT ( 'NONE',  ( 0.000000000000000000, 0.000000000000000000, -8.400000000000018119 ) ) ;
#8026=ORIENTED_EDGE ( 'NONE', *, *, #7198, .F. ) ;
#8032=CARTESIAN_POINT ( 'NONE',  ( 8.000000000000117240, 4.618802153517009401, -7.685468820183672278 ) ) ;
#8033=AXIS2_PLACEMENT_3D ( 'NONE', #4559, #4039, #687 ) ;
#8045=CARTESIAN_POINT ( 'NONE',  ( -7.999999999999894307, 1.572549600175511042, -0.06894455525505825688 ) ) ;
#8064=ORIENTED_EDGE ( 'NONE', *, *, #3590, .T. ) ;
#8067=CLOSED_SHELL ( 'NONE', ( #4702, #4114, #5040, #1080, #2875, #5511, #6541, #2725, #4073, #2596, #536, #8131, #5019, #5982, #5396, #4595, #7182, #5391, #5897, #4327, #3264, #2208 ) ) ;
#8071=DIRECTION ( 'NONE',  ( 0.000000000000000000, 0.000000000000000000, -1.000000000000000000 ) ) ;
#8072=ORIENTED_EDGE ( 'NONE', *, *, #2672, .T. ) ;
#8074=MECHANICAL_DESIGN_GEOMETRIC_PRESENTATION_REPRESENTATION('',(#8211),#8487);
#8112=EDGE_LOOP ( 'NONE', ( #4099, #2225 ) ) ;
#8116=CARTESIAN_POINT ( 'NONE',  ( 0.000000000000000000, 0.000000000000000000, 0.000000000000000000 ) ) ;
#8131=ADVANCED_FACE ( 'NONE', ( #6382 ), #1541, .T. ) ;
#8140=EDGE_CURVE ( 'NONE', #650, #3046, #5015, .T. ) ;
#8141=AXIS2_PLACEMENT_3D ( 'NONE', #1821, #6410, #444 ) ;
#8151=FACE_OUTER_BOUND ( 'NONE', #2543, .T. ) ;
#8168=DIRECTION ( 'NONE',  ( 0.000000000000000000, 0.000000000000000000, 1.000000000000000000 ) ) ;
#8175=DIRECTION ( 'NONE',  ( 0.000000000000000000, 0.000000000000000000, 1.000000000000000000 ) ) ;
#8211=STYLED_ITEM('',(#8670),#40);
#8224=PRODUCT_DEFINITION_CONTEXT ( 'detailed design', #6817, 'design' ) ;
#8235=AXIS2_PLACEMENT_3D ( 'NONE', #3033, #5760, #5720 ) ;
#8245=ORIENTED_EDGE ( 'NONE', *, *, #7365, .T. ) ;
#8289=CARTESIAN_POINT ( 'NONE',  ( 0.000000000000000000, 0.000000000000000000, 0.000000000000000000 ) ) ;
#8304=EDGE_LOOP ( 'NONE', ( #6857, #1820, #7603 ) ) ;
#8313=ORIENTED_EDGE ( 'NONE', *, *, #576, .T. ) ;
#8319=DIRECTION ( 'NONE',  ( -1.000000000000000000, -8.881784197001244435E-16, 0.000000000000000000 ) ) ;
#8321=DIRECTION ( 'NONE',  ( 0.9237280213470678847, 0.3830490080632384942, 0.000000000000000000 ) ) ;
#8326=ORIENTED_EDGE ( 'NONE', *, *, #6937, .T. ) ;
#8359=CARTESIAN_POINT ( 'NONE',  ( 2.220446049250313081E-13, -9.237604307034242623, -8.400000000000018119 ) ) ;
#8365=EDGE_LOOP ( 'NONE', ( #655, #7522, #1274 ) ) ;
#8397=CARTESIAN_POINT ( 'NONE',  ( -3.660532965668688909, 7.124194613927615549, -8.400000000000062528 ) ) ;
#8403=CARTESIAN_POINT ( 'NONE',  ( 8.000000000000229150, 4.618802153516954334, -8.400000000000018119 ) ) ;
#8405=B_SPLINE_CURVE_WITH_KNOTS ( 'NONE', 3,
 ( #5315, #2003, #2571, #5226, #1350, #7354 ),
 .UNSPECIFIED., .F., .F.,
 ( 4, 2, 4 ),
 ( 2.380731631918174131E-07, 0.002336973833157790156, 0.004673709593152389034 ),
 .UNSPECIFIED. ) ;
#8413=CARTESIAN_POINT ( 'NONE',  ( 8.000000000000234479, -0.7805016046292178045, -8.399999999999876010 ) ) ;
#8429=CARTESIAN_POINT ( 'NONE',  ( -1.310872448937805634, 8.480771745766437775, -0.3173508448886594446 ) ) ;
#8445=ORIENTED_EDGE ( 'NONE', *, *, #2618, .T. ) ;
#8446=DIRECTION ( 'NONE',  ( -1.000000000000000000, -8.881784197001244435E-16, 0.000000000000000000 ) ) ;
#8470=EDGE_CURVE ( 'NONE', #3749, #902, #2530, .T. ) ;
#8487=( GEOMETRIC_REPRESENTATION_CONTEXT ( 3 ) GLOBAL_UNCERTAINTY_ASSIGNED_CONTEXT ( ( #6834 ) ) GLOBAL_UNIT_ASSIGNED_CONTEXT ( ( #4823, #819, #4163 ) ) REPRESENTATION_CONTEXT ( 'NONE', 'WORKASPACE' ) );
#8505=VERTEX_POINT ( 'NONE', #6556 ) ;
#8508=DIRECTION ( 'NONE',  ( 0.000000000000000000, 0.000000000000000000, 1.000000000000000000 ) ) ;
#8520=CARTESIAN_POINT ( 'NONE',  ( 8.000000000000232703, 0.7809653281575149597, -1.284508523852201883E-13 ) ) ;
#8542=ORIENTED_EDGE ( 'NONE', *, *, #5373, .F. ) ;
#8556=B_SPLINE_CURVE_WITH_KNOTS ( 'NONE', 3,
 ( #388, #7128, #3163, #7049, #6400, #1767, #433, #3779 ),
 .UNSPECIFIED., .F., .F.,
 ( 4, 2, 2, 4 ),
 ( 0.004673709593152389034, 0.005837709341827845497, 0.007001709090503301092, 0.009329708587854212282 ),
 .UNSPECIFIED. ) ;
#8562=CARTESIAN_POINT ( 'NONE',  ( 8.000000000000232703, 1.572549600175502604, -0.06894455525524925688 ) ) ;
#8585=CARTESIAN_POINT ( 'NONE',  ( 8.000000000000229150, 3.871967595402076689, -7.901061386767455730 ) ) ;
#8664=COLOUR_RGB('Black',0.12,0.14,0.17);
#8665=FILL_AREA_STYLE_COLOUR('',#8664);
#8666=FILL_AREA_STYLE('',(#8665));
#8667=SURFACE_STYLE_FILL_AREA(#8666);
#8668=SURFACE_SIDE_STYLE('',(#8667));
#8669=SURFACE_STYLE_USAGE(.BOTH.,#8668);
#8670=PRESENTATION_STYLE_ASSIGNMENT((#8669));
ENDSEC;
END-ISO-10303-21;
